ISO-10303-21;
HEADER;
/* Generated by software containing ST-Developer
 * from STEP Tools, Inc. (www.steptools.com) 
 */

FILE_DESCRIPTION(
/* description */ ('Cable chain and bracket set'),
/* implementation_level */ '2;1');

FILE_NAME(
/* name */ 'Hinge bearing sleeve__PD6068.step',
/* time_stamp */ '2026-10-29T17:19:47-07:00',
/* author */ (''),
/* organization */ (''),
/* preprocessor_version */ 'ST-DEVELOPER v20.2',
/* originating_system */ 'Autodesk Translation Framework v15.17.0.0',
/* authorisation */ '');

FILE_SCHEMA (('AUTOMOTIVE_DESIGN { 1 0 10303 214 3 1 1 }'));
ENDSEC;

DATA;
#10=MECHANICAL_DESIGN_GEOMETRIC_PRESENTATION_REPRESENTATION('',(#339),#5929);
#313=SHAPE_REPRESENTATION_RELATIONSHIP('SRR','None',#6044,#326);
#326=ADVANCED_BREP_SHAPE_REPRESENTATION('',(#352),#5911);
#339=STYLED_ITEM('',(#6220),#352);
#352=MANIFOLD_SOLID_BREP('Body1',#3333);
#375=FACE_BOUND('',#780,.T.);
#376=FACE_BOUND('',#782,.T.);
#443=PLANE('',#3534);
#444=PLANE('',#3535);
#583=FACE_OUTER_BOUND('',#777,.T.);
#584=FACE_OUTER_BOUND('',#778,.T.);
#585=FACE_OUTER_BOUND('',#779,.T.);
#586=FACE_OUTER_BOUND('',#781,.T.);
#777=EDGE_LOOP('',(#2537,#2538,#2539,#2540));
#778=EDGE_LOOP('',(#2541,#2542,#2543,#2544));
#779=EDGE_LOOP('',(#2545));
#780=EDGE_LOOP('',(#2546));
#781=EDGE_LOOP('',(#2547));
#782=EDGE_LOOP('',(#2548));
#1033=LINE('',#5156,#1293);
#1034=LINE('',#5162,#1294);
#1293=VECTOR('',#4130,0.310000000000035);
#1294=VECTOR('',#4137,0.400000000000046);
#1487=CIRCLE('',#3529,0.310000000000035);
#1488=CIRCLE('',#3530,0.310000000000035);
#1489=CIRCLE('',#3532,0.400000000000046);
#1490=CIRCLE('',#3533,0.400000000000046);
#1649=VERTEX_POINT('',#5153);
#1650=VERTEX_POINT('',#5155);
#1651=VERTEX_POINT('',#5159);
#1652=VERTEX_POINT('',#5161);
#1969=EDGE_CURVE('',#1649,#1649,#1487,.T.);
#1970=EDGE_CURVE('',#1649,#1650,#1033,.T.);
#1971=EDGE_CURVE('',#1650,#1650,#1488,.T.);
#1972=EDGE_CURVE('',#1651,#1651,#1489,.T.);
#1973=EDGE_CURVE('',#1651,#1652,#1034,.T.);
#1974=EDGE_CURVE('',#1652,#1652,#1490,.T.);
#2537=ORIENTED_EDGE('',*,*,#1969,.F.);
#2538=ORIENTED_EDGE('',*,*,#1970,.T.);
#2539=ORIENTED_EDGE('',*,*,#1971,.T.);
#2540=ORIENTED_EDGE('',*,*,#1970,.F.);
#2541=ORIENTED_EDGE('',*,*,#1972,.F.);
#2542=ORIENTED_EDGE('',*,*,#1973,.T.);
#2543=ORIENTED_EDGE('',*,*,#1974,.T.);
#2544=ORIENTED_EDGE('',*,*,#1973,.F.);
#2545=ORIENTED_EDGE('',*,*,#1972,.T.);
#2546=ORIENTED_EDGE('',*,*,#1969,.T.);
#2547=ORIENTED_EDGE('',*,*,#1974,.F.);
#2548=ORIENTED_EDGE('',*,*,#1971,.F.);
#3115=CYLINDRICAL_SURFACE('',#3528,0.310000000000035);
#3116=CYLINDRICAL_SURFACE('',#3531,0.400000000000046);
#3205=ADVANCED_FACE('',(#583),#3115,.F.);
#3206=ADVANCED_FACE('',(#584),#3116,.T.);
#3207=ADVANCED_FACE('',(#585,#375),#443,.T.);
#3208=ADVANCED_FACE('',(#586,#376),#444,.F.);
#3333=CLOSED_SHELL('',(#3205,#3206,#3207,#3208));
#3527=AXIS2_PLACEMENT_3D('',#5151,#4124,#4125);
#3528=AXIS2_PLACEMENT_3D('',#5152,#4126,#4127);
#3529=AXIS2_PLACEMENT_3D('',#5154,#4128,#4129);
#3530=AXIS2_PLACEMENT_3D('',#5157,#4131,#4132);
#3531=AXIS2_PLACEMENT_3D('',#5158,#4133,#4134);
#3532=AXIS2_PLACEMENT_3D('',#5160,#4135,#4136);
#3533=AXIS2_PLACEMENT_3D('',#5163,#4138,#4139);
#3534=AXIS2_PLACEMENT_3D('',#5164,#4140,#4141);
#3535=AXIS2_PLACEMENT_3D('',#5165,#4142,#4143);
#4124=DIRECTION('axis',(0.,0.,1.));
#4125=DIRECTION('refdir',(1.,0.,0.));
#4126=DIRECTION('center_axis',(-6.12323399573548E-17,1.,4.78224871431377E-30));
#4127=DIRECTION('ref_axis',(0.939692587475203,5.75395759716863E-17,0.342020234846066));
#4128=DIRECTION('center_axis',(6.12323399573548E-17,-1.,-4.78224871431377E-30));
#4129=DIRECTION('ref_axis',(0.939692587475203,5.75395759716863E-17,0.342020234846066));
#4130=DIRECTION('',(6.12323399573548E-17,-1.,-4.78224871431377E-30));
#4131=DIRECTION('center_axis',(6.12323399573548E-17,-1.,-4.78224871431377E-30));
#4132=DIRECTION('ref_axis',(0.939692587475203,5.75395759716863E-17,0.342020234846066));
#4133=DIRECTION('center_axis',(-6.12323399573548E-17,1.,4.78224871431377E-30));
#4134=DIRECTION('ref_axis',(0.939692587475203,5.75395759716863E-17,0.342020234846066));
#4135=DIRECTION('center_axis',(-6.12323399573548E-17,1.,4.78224871431377E-30));
#4136=DIRECTION('ref_axis',(0.939692587475203,5.75395759716863E-17,0.342020234846066));
#4137=DIRECTION('',(6.12323399573548E-17,-1.,-4.78224871431377E-30));
#4138=DIRECTION('center_axis',(-6.12323399573548E-17,1.,4.78224871431377E-30));
#4139=DIRECTION('ref_axis',(0.939692587475203,5.75395759716863E-17,0.342020234846066));
#4140=DIRECTION('center_axis',(-6.12323399573548E-17,1.,4.78224871431377E-30));
#4141=DIRECTION('ref_axis',(0.939692587475203,5.75395759716863E-17,0.342020234846066));
#4142=DIRECTION('center_axis',(-6.12323399573548E-17,1.,4.78224871431377E-30));
#4143=DIRECTION('ref_axis',(0.939692587475203,5.75395759716863E-17,0.342020234846066));
#5151=CARTESIAN_POINT('',(0.,0.,0.));
#5152=CARTESIAN_POINT('Origin',(2.34923146868827,-1.56000000000018,3.85505058711526));
#5153=CARTESIAN_POINT('',(2.05792676657093,1.56000000000018,3.74902431431297));
#5154=CARTESIAN_POINT('Origin',(2.34923146868827,1.56000000000018,3.85505058711526));
#5155=CARTESIAN_POINT('',(2.05792676657093,-1.56000000000018,3.74902431431297));
#5156=CARTESIAN_POINT('',(2.05792676657093,-1.56000000000018,3.74902431431297));
#5157=CARTESIAN_POINT('Origin',(2.34923146868827,-1.56000000000018,3.85505058711526));
#5158=CARTESIAN_POINT('Origin',(2.34923146868827,-1.56000000000018,3.85505058711526));
#5159=CARTESIAN_POINT('',(1.97335443369815,1.56000000000018,3.71824249317682));
#5160=CARTESIAN_POINT('Origin',(2.34923146868827,1.56000000000018,3.85505058711526));
#5161=CARTESIAN_POINT('',(1.97335443369815,-1.56000000000018,3.71824249317682));
#5162=CARTESIAN_POINT('',(1.97335443369815,-1.56000000000018,3.71824249317682));
#5163=CARTESIAN_POINT('Origin',(2.34923146868827,-1.56000000000018,3.85505058711526));
#5164=CARTESIAN_POINT('Origin',(2.34923146868827,1.56000000000018,3.85505058711526));
#5165=CARTESIAN_POINT('Origin',(2.34923146868827,-1.56000000000018,3.85505058711526));
#5887=UNCERTAINTY_MEASURE_WITH_UNIT(LENGTH_MEASURE(0.001),#5930,
'DISTANCE_ACCURACY_VALUE',
'Maximum model space distance between geometric entities at asserted c
onnectivities');
#5905=UNCERTAINTY_MEASURE_WITH_UNIT(LENGTH_MEASURE(0.001),#5930,
'DISTANCE_ACCURACY_VALUE',
'Maximum model space distance between geometric entities at asserted c
onnectivities');
#5911=(
GEOMETRIC_REPRESENTATION_CONTEXT(3)
GLOBAL_UNCERTAINTY_ASSIGNED_CONTEXT((#5887))
GLOBAL_UNIT_ASSIGNED_CONTEXT((#5930,#5932,#5933))
REPRESENTATION_CONTEXT('','3D')
);
#5929=(
GEOMETRIC_REPRESENTATION_CONTEXT(3)
GLOBAL_UNCERTAINTY_ASSIGNED_CONTEXT((#5905))
GLOBAL_UNIT_ASSIGNED_CONTEXT((#5930,#5932,#5933))
REPRESENTATION_CONTEXT('','3D')
);
#5930=(
LENGTH_UNIT()
NAMED_UNIT(*)
SI_UNIT(.CENTI.,.METRE.)
);
#5932=(
NAMED_UNIT(*)
PLANE_ANGLE_UNIT()
SI_UNIT($,.RADIAN.)
);
#5933=(
NAMED_UNIT(*)
SI_UNIT($,.STERADIAN.)
SOLID_ANGLE_UNIT()
);
#5939=SHAPE_DEFINITION_REPRESENTATION(#5962,#6044);
#5962=PRODUCT_DEFINITION_SHAPE('',$,#6068);
#6044=SHAPE_REPRESENTATION('',(#3527),#5911);
#6062=PRODUCT_DEFINITION_CONTEXT('part definition',#6133,'design');
#6068=PRODUCT_DEFINITION('Hinge bearing sleeve','Hinge bearing sleeve',
#6091,#6062);
#6091=PRODUCT_DEFINITION_FORMATION('',$,#6140);
#6133=APPLICATION_CONTEXT(
'Core Data for Automotive Mechanical Design Process');
#6134=PRODUCT_CONTEXT('part definition',#6133,'mechanical');
#6140=PRODUCT('Hinge bearing sleeve','Hinge bearing sleeve',
'Hinge bearing sleeve',(#6134));
#6214=COLOUR_RGB('Grey',0.48,0.52,0.57);
#6215=FILL_AREA_STYLE_COLOUR('',#6214);
#6216=FILL_AREA_STYLE('',(#6215));
#6217=SURFACE_STYLE_FILL_AREA(#6216);
#6218=SURFACE_SIDE_STYLE('',(#6217));
#6219=SURFACE_STYLE_USAGE(.BOTH.,#6218);
#6220=PRESENTATION_STYLE_ASSIGNMENT((#6219));
ENDSEC;
END-ISO-10303-21;
